ISO-10303-21;
HEADER;
FILE_DESCRIPTION (('STEP AP214'),
    '1' );
FILE_NAME ('needle roller bearing_nm_iso_ISO 3030 - 15C2230 - Full,SI,AC,Full.step',
    '2026-10-08T11:45:07',
    ( '' ),
    ( '' ),
    'SwSTEP 2.0',
    'SolidWorks 2026',
    '' );
FILE_SCHEMA (( 'AUTOMOTIVE_DESIGN' ));
ENDSEC;

DATA;
#1=TOROIDAL_SURFACE ( 'NONE', #14678, 14.91999999999999815, 0.08000000000000020983 ) ;
#32=ORIENTED_EDGE ( 'NONE', *, *, #36401, .F. ) ;
#53=SURFACE_SIDE_STYLE ('',( #30002 ) ) ;
#113=PRODUCT ( 'needle roller bearing_nm_iso_ISO 3030 - 15C2230 - Full,SI,AC,Full', 'needle roller bearing_nm_iso_ISO 3030 - 15C2230 - Full,SI,AC,Full', '', ( #9801 ) ) ;
#181=AXIS2_PLACEMENT_3D ( 'NONE', #33308, #3602, #40474 ) ;
#265=FILL_AREA_STYLE_COLOUR ( '', #39229 ) ;
#349=DIRECTION ( 'NONE',  ( -1.000000000000000000, -0.000000000000000000, -0.000000000000000000 ) ) ;
#364=ADVANCED_FACE ( 'NONE', ( #3690, #17069 ), #21009, .F. ) ;
#461=DIRECTION ( 'NONE',  ( -1.000000000000000000, -0.000000000000000000, -0.000000000000000000 ) ) ;
#585=FACE_OUTER_BOUND ( 'NONE', #22797, .T. ) ;
#634=DIRECTION ( 'NONE',  ( 0.000000000000000000, 0.000000000000000000, 1.000000000000000000 ) ) ;
#679=DIRECTION ( 'NONE',  ( 0.000000000000000000, 0.000000000000000000, -1.000000000000000000 ) ) ;
#705=TOROIDAL_SURFACE ( 'NONE', #25164, 11.08000000000000007, 0.07999999999999934941 ) ;
#760=PRODUCT_DEFINITION_CONTEXT ( 'detailed design', #10016, 'design' ) ;
#764=DIRECTION ( 'NONE',  ( 0.000000000000000000, 0.000000000000000000, 1.000000000000000000 ) ) ;
#767=APPLICATION_CONTEXT ( 'automotive_design' ) ;
#817=CARTESIAN_POINT ( 'NONE',  ( 8.999999999999998224, 0.000000000000000000, 0.000000000000000000 ) ) ;
#833=AXIS2_PLACEMENT_3D ( 'NONE', #2147, #5444, #11574 ) ;
#850=DIRECTION ( 'NONE',  ( -1.000000000000000000, 0.000000000000000000, -0.000000000000000000 ) ) ;
#853=ORIENTED_EDGE ( 'NONE', *, *, #28742, .T. ) ;
#872=FACE_OUTER_BOUND ( 'NONE', #36740, .T. ) ;
#892=ORIENTED_EDGE ( 'NONE', *, *, #25986, .F. ) ;
#970=CIRCLE ( 'NONE', #29563, 11.00000000000000000 ) ;
#1088=ADVANCED_FACE ( 'NONE', ( #42882 ), #16099, .T. ) ;
#1091=EDGE_CURVE ( 'NONE', #37611, #35369, #9602, .T. ) ;
#1177=FACE_OUTER_BOUND ( 'NONE', #17116, .T. ) ;
#1209=DIRECTION ( 'NONE',  ( 0.000000000000000000, 0.000000000000000000, 1.000000000000000000 ) ) ;
#1285=AXIS2_PLACEMENT_3D ( 'NONE', #2931, #42870, #13027 ) ;
#1313=ORIENTED_EDGE ( 'NONE', *, *, #34877, .F. ) ;
#1366=EDGE_CURVE ( 'NONE', #15009, #26006, #30046, .T. ) ;
#1424=CIRCLE ( 'NONE', #27206, 11.08000000000000007 ) ;
#1509=CARTESIAN_POINT ( 'NONE',  ( -12.69999999999999929, 0.000000000000000000, 0.000000000000000000 ) ) ;
#1793=EDGE_LOOP ( 'NONE', ( #14472, #36351, #5138, #29212 ) ) ;
#1820=VECTOR ( 'NONE', #22340, 1000.000000000000000 ) ;
#1881=CARTESIAN_POINT ( 'NONE',  ( -17.77999999999999758, 0.000000000000000000, 14.99999999999999822 ) ) ;
#1999=AXIS2_PLACEMENT_3D ( 'NONE', #2718, #33289, #29180 ) ;
#2064=CARTESIAN_POINT ( 'NONE',  ( -8.920000000000003482, 0.000000000000000000, 14.91999999999999815 ) ) ;
#2091=CARTESIAN_POINT ( 'NONE',  ( -9.000000000000005329, 0.000000000000000000, -12.59999999999999964 ) ) ;
#2107=ADVANCED_FACE ( 'NONE', ( #18868, #2842 ), #3047, .T. ) ;
#2147=CARTESIAN_POINT ( 'NONE',  ( 8.999999999999998224, 0.000000000000000000, 0.000000000000000000 ) ) ;
#2228=CIRCLE ( 'NONE', #833, 14.91999999999999993 ) ;
#2246=ORIENTED_EDGE ( 'NONE', *, *, #35440, .F. ) ;
#2262=VERTEX_POINT ( 'NONE', #20150 ) ;
#2273=EDGE_LOOP ( 'NONE', ( #26089, #30626, #3550, #8568 ) ) ;
#2393=DIRECTION ( 'NONE',  ( 0.000000000000000000, 0.000000000000000000, 1.000000000000000000 ) ) ;
#2411=DIRECTION ( 'NONE',  ( 0.000000000000000000, 0.000000000000000000, 1.000000000000000000 ) ) ;
#2527=AXIS2_PLACEMENT_3D ( 'NONE', #31144, #349, #3621 ) ;
#2573=LINE ( 'NONE', #23132, #39850 ) ;
#2718=CARTESIAN_POINT ( 'NONE',  ( 8.919999999999999929, 0.000000000000000000, 11.08000000000000007 ) ) ;
#2767=EDGE_CURVE ( 'NONE', #35289, #2262, #35243, .T. ) ;
#2800=CARTESIAN_POINT ( 'NONE',  ( -8.920000000000003482, 1.356908653455267209E-15, -11.08000000000000007 ) ) ;
#2842=FACE_BOUND ( 'NONE', #18369, .T. ) ;
#2921=EDGE_LOOP ( 'NONE', ( #3255, #21732, #7590, #19568 ) ) ;
#2931=CARTESIAN_POINT ( 'NONE',  ( -9.000000000000005329, 0.000000000000000000, 0.000000000000000000 ) ) ;
#2942=CARTESIAN_POINT ( 'NONE',  ( 8.919999999999996376, 0.000000000000000000, 14.91999999999999815 ) ) ;
#2943=DIRECTION ( 'NONE',  ( 1.000000000000000000, 0.000000000000000000, 0.000000000000000000 ) ) ;
#2944=EDGE_CURVE ( 'NONE', #19475, #30260, #41418, .T. ) ;
#2964=MECHANICAL_DESIGN_GEOMETRIC_PRESENTATION_REPRESENTATION('',(#19081),#14178);
#3046=CYLINDRICAL_SURFACE ( 'NONE', #12012, 14.99999999999999822 ) ;
#3047=PLANE ( 'NONE',  #26230 ) ;
#3089=CARTESIAN_POINT ( 'NONE',  ( -9.000000000000005329, 0.000000000000000000, 0.000000000000000000 ) ) ;
#3111=EDGE_LOOP ( 'NONE', ( #33066, #27584 ) ) ;
#3112=FILL_AREA_STYLE ('',( #265 ) ) ;
#3196=ORIENTED_EDGE ( 'NONE', *, *, #35724, .T. ) ;
#3215=DIRECTION ( 'NONE',  ( 1.000000000000000000, 0.000000000000000000, 0.000000000000000000 ) ) ;
#3255=ORIENTED_EDGE ( 'NONE', *, *, #35440, .T. ) ;
#3288=DIRECTION ( 'NONE',  ( 0.000000000000000000, 0.000000000000000000, 1.000000000000000000 ) ) ;
#3369=DIRECTION ( 'NONE',  ( 0.000000000000000000, 0.000000000000000000, 1.000000000000000000 ) ) ;
#3441=CARTESIAN_POINT ( 'NONE',  ( -8.920000000000003482, 0.000000000000000000, 0.000000000000000000 ) ) ;
#3443=AXIS2_PLACEMENT_3D ( 'NONE', #2942, #10158, #19591 ) ;
#3456=ORIENTED_EDGE ( 'NONE', *, *, #4256, .T. ) ;
#3517=CARTESIAN_POINT ( 'NONE',  ( 9.999999999999998224, 0.000000000000000000, 0.000000000000000000 ) ) ;
#3537=CIRCLE ( 'NONE', #16138, 12.59999999999999964 ) ;
#3550=ORIENTED_EDGE ( 'NONE', *, *, #10461, .T. ) ;
#3566=CARTESIAN_POINT ( 'NONE',  ( 8.919999999999998153, 0.000000000000000000, 11.00000000000000000 ) ) ;
#3602=DIRECTION ( 'NONE',  ( -1.000000000000000000, -0.000000000000000000, -0.000000000000000000 ) ) ;
#3621=DIRECTION ( 'NONE',  ( 0.000000000000000000, 0.000000000000000000, 1.000000000000000000 ) ) ;
#3629=DIRECTION ( 'NONE',  ( -1.000000000000000000, -0.000000000000000000, -0.000000000000000000 ) ) ;
#3632=AXIS2_PLACEMENT_3D ( 'NONE', #11823, #41015, #11162 ) ;
#3690=FACE_OUTER_BOUND ( 'NONE', #37695, .T. ) ;
#3728=DIRECTION ( 'NONE',  ( 0.000000000000000000, 0.000000000000000000, 1.000000000000000000 ) ) ;
#3756=( LENGTH_UNIT ( ) NAMED_UNIT ( * ) SI_UNIT ( .MILLI., .METRE. ) );
#3764=CIRCLE ( 'NONE', #17770, 12.59999999999999964 ) ;
#3852=CARTESIAN_POINT ( 'NONE',  ( 0.000000000000000000, 0.000000000000000000, 0.000000000000000000 ) ) ;
#3876=DIRECTION ( 'NONE',  ( 1.000000000000000000, 0.000000000000000000, 0.000000000000000000 ) ) ;
#3929=DIRECTION ( 'NONE',  ( -1.000000000000000000, -0.000000000000000000, -0.000000000000000000 ) ) ;
#3974=EDGE_CURVE ( 'NONE', #37158, #39523, #10131, .T. ) ;
#4023=CARTESIAN_POINT ( 'NONE',  ( -8.920000000000003482, 0.000000000000000000, 0.000000000000000000 ) ) ;
#4031=VECTOR ( 'NONE', #40676, 1000.000000000000000 ) ;
#4126=CARTESIAN_POINT ( 'NONE',  ( 8.919999999999998153, 0.000000000000000000, 0.000000000000000000 ) ) ;
#4231=TOROIDAL_SURFACE ( 'NONE', #31428, 14.91999999999999815, 0.08000000000000020983 ) ;
#4256=EDGE_CURVE ( 'NONE', #7493, #25155, #38870, .T. ) ;
#4259=CARTESIAN_POINT ( 'NONE',  ( -9.000000000000005329, 1.641026710857453510E-15, 13.40000000000000213 ) ) ;
#4271=CYLINDRICAL_SURFACE ( 'NONE', #36759, 11.00000000000000000 ) ;
#4306=DIRECTION ( 'NONE',  ( -1.000000000000000000, -0.000000000000000000, -0.000000000000000000 ) ) ;
#4341=DIRECTION ( 'NONE',  ( 1.000000000000000000, 0.000000000000000000, 0.000000000000000000 ) ) ;
#4397=EDGE_CURVE ( 'NONE', #13782, #18607, #37354, .T. ) ;
#4428=ORIENTED_EDGE ( 'NONE', *, *, #5908, .F. ) ;
#4472=DIRECTION ( 'NONE',  ( -1.000000000000000000, -0.000000000000000000, -0.000000000000000000 ) ) ;
#4567=ORIENTED_EDGE ( 'NONE', *, *, #9643, .T. ) ;
#4585=CARTESIAN_POINT ( 'NONE',  ( -9.000000000000007105, 0.000000000000000000, 0.000000000000000000 ) ) ;
#4656=VECTOR ( 'NONE', #29313, 1000.000000000000000 ) ;
#4846=DIRECTION ( 'NONE',  ( 0.000000000000000000, 0.000000000000000000, -1.000000000000000000 ) ) ;
#4857=EDGE_CURVE ( 'NONE', #19972, #30408, #24464, .T. ) ;
#4861=VERTEX_POINT ( 'NONE', #30049 ) ;
#4959=DIRECTION ( 'NONE',  ( 0.000000000000000000, -1.224646799147343346E-16, 1.000000000000000000 ) ) ;
#4997=CARTESIAN_POINT ( 'NONE',  ( -12.69999999999999929, 0.000000000000000000, 0.000000000000000000 ) ) ;
#4998=ADVANCED_FACE ( 'NONE', ( #17838 ), #30756, .T. ) ;
#5086=AXIS2_PLACEMENT_3D ( 'NONE', #16088, #12391, #9083 ) ;
#5131=( LENGTH_UNIT ( ) NAMED_UNIT ( * ) SI_UNIT ( .MILLI., .METRE. ) );
#5138=ORIENTED_EDGE ( 'NONE', *, *, #2767, .T. ) ;
#5157=CARTESIAN_POINT ( 'NONE',  ( 9.999999999999998224, 0.000000000000000000, 0.000000000000000000 ) ) ;
#5262=CIRCLE ( 'NONE', #23381, 13.40000000000000036 ) ;
#5326=CARTESIAN_POINT ( 'NONE',  ( 9.999999999999998224, 0.000000000000000000, 0.000000000000000000 ) ) ;
#5385=ORIENTED_EDGE ( 'NONE', *, *, #20734, .F. ) ;
#5443=CIRCLE ( 'NONE', #36098, 14.99999999999999822 ) ;
#5444=DIRECTION ( 'NONE',  ( -1.000000000000000000, -0.000000000000000000, -0.000000000000000000 ) ) ;
#5471=VERTEX_POINT ( 'NONE', #41505 ) ;
#5513=DIRECTION ( 'NONE',  ( 1.000000000000000000, 0.000000000000000000, 0.000000000000000000 ) ) ;
#5612=ORIENTED_EDGE ( 'NONE', *, *, #34877, .T. ) ;
#5690=VERTEX_POINT ( 'NONE', #25822 ) ;
#5697=VERTEX_POINT ( 'NONE', #33617 ) ;
#5731=LINE ( 'NONE', #32352, #4656 ) ;
#5908=EDGE_CURVE ( 'NONE', #37158, #27138, #1424, .T. ) ;
#5920=FACE_OUTER_BOUND ( 'NONE', #30599, .T. ) ;
#5987=DIRECTION ( 'NONE',  ( 0.000000000000000000, 0.000000000000000000, -1.000000000000000000 ) ) ;
#6148=DIRECTION ( 'NONE',  ( 0.000000000000000000, 0.000000000000000000, -1.000000000000000000 ) ) ;
#6204=CARTESIAN_POINT ( 'NONE',  ( -9.000000000000005329, 0.000000000000000000, 0.000000000000000000 ) ) ;
#6287=ORIENTED_EDGE ( 'NONE', *, *, #24453, .T. ) ;
#6367=FACE_OUTER_BOUND ( 'NONE', #11408, .T. ) ;
#6393=AXIS2_PLACEMENT_3D ( 'NONE', #19702, #32967, #26443 ) ;
#6499=FACE_OUTER_BOUND ( 'NONE', #31306, .T. ) ;
#6548=FACE_OUTER_BOUND ( 'NONE', #13207, .T. ) ;
#6589=CARTESIAN_POINT ( 'NONE',  ( -9.000000000000005329, 1.543054966925665076E-15, 12.59999999999999964 ) ) ;
#6726=CARTESIAN_POINT ( 'NONE',  ( 8.919999999999999929, 0.000000000000000000, 0.000000000000000000 ) ) ;
#6810=EDGE_CURVE ( 'NONE', #27138, #5471, #19804, .T. ) ;
#6883=EDGE_LOOP ( 'NONE', ( #26429, #32343, #3196, #18251 ) ) ;
#6937=DIRECTION ( 'NONE',  ( 0.000000000000000000, 0.000000000000000000, -1.000000000000000000 ) ) ;
#6991=EDGE_CURVE ( 'NONE', #27839, #30260, #18880, .T. ) ;
#7268=SURFACE_SIDE_STYLE ('',( #31289 ) ) ;
#7429=TOROIDAL_SURFACE ( 'NONE', #26941, 14.91999999999999815, 0.08000000000000020983 ) ;
#7442=DIRECTION ( 'NONE',  ( 0.000000000000000000, 0.000000000000000000, 1.000000000000000000 ) ) ;
#7461=ORIENTED_EDGE ( 'NONE', *, *, #22463, .F. ) ;
#7493=VERTEX_POINT ( 'NONE', #9816 ) ;
#7525=DIRECTION ( 'NONE',  ( 1.000000000000000000, 0.000000000000000000, 0.000000000000000000 ) ) ;
#7554=AXIS2_PLACEMENT_3D ( 'NONE', #4126, #33816, #634 ) ;
#7563=CARTESIAN_POINT ( 'NONE',  ( -9.000000000000005329, 0.000000000000000000, 0.000000000000000000 ) ) ;
#7590=ORIENTED_EDGE ( 'NONE', *, *, #17042, .T. ) ;
#7631=DIRECTION ( 'NONE',  ( 0.000000000000000000, 0.000000000000000000, -1.000000000000000000 ) ) ;
#7761=CARTESIAN_POINT ( 'NONE',  ( 8.919999999999994600, 0.000000000000000000, 0.000000000000000000 ) ) ;
#7802=ORIENTED_EDGE ( 'NONE', *, *, #8418, .F. ) ;
#7850=ORIENTED_EDGE ( 'NONE', *, *, #35770, .F. ) ;
#7905=ORIENTED_EDGE ( 'NONE', *, *, #6810, .T. ) ;
#7913=EDGE_LOOP ( 'NONE', ( #41299, #30596, #33138, #853 ) ) ;
#8066=AXIS2_PLACEMENT_3D ( 'NONE', #18068, #27853, #23778 ) ;
#8088=ADVANCED_FACE ( 'NONE', ( #585 ), #4231, .T. ) ;
#8118=CARTESIAN_POINT ( 'NONE',  ( -10.00000000000000178, 0.000000000000000000, 0.000000000000000000 ) ) ;
#8278=DIRECTION ( 'NONE',  ( 1.000000000000000000, 0.000000000000000000, 0.000000000000000000 ) ) ;
#8335=CARTESIAN_POINT ( 'NONE',  ( -10.00000000000000178, 0.000000000000000000, -13.40000000000000036 ) ) ;
#8345=CARTESIAN_POINT ( 'NONE',  ( -12.69999999999999929, 0.000000000000000000, -13.40000000000000213 ) ) ;
#8418=EDGE_CURVE ( 'NONE', #35542, #7493, #3537, .T. ) ;
#8568=ORIENTED_EDGE ( 'NONE', *, *, #19362, .F. ) ;
#8572=ORIENTED_EDGE ( 'NONE', *, *, #35770, .T. ) ;
#8580=DIRECTION ( 'NONE',  ( 0.000000000000000000, 0.000000000000000000, -1.000000000000000000 ) ) ;
#8645=ORIENTED_EDGE ( 'NONE', *, *, #2767, .F. ) ;
#8708=EDGE_LOOP ( 'NONE', ( #24426, #39673, #892, #1313 ) ) ;
#8723=AXIS2_PLACEMENT_3D ( 'NONE', #22805, #26269, #3728 ) ;
#8726=EDGE_LOOP ( 'NONE', ( #27054, #14687 ) ) ;
#8772=AXIS2_PLACEMENT_3D ( 'NONE', #7563, #21353, #24403 ) ;
#8778=DIRECTION ( 'NONE',  ( -1.000000000000000000, 0.000000000000000000, -0.000000000000000000 ) ) ;
#8832=VECTOR ( 'NONE', #37668, 1000.000000000000000 ) ;
#8872=CARTESIAN_POINT ( 'NONE',  ( 8.999999999999998224, 0.000000000000000000, 0.000000000000000000 ) ) ;
#8878=AXIS2_PLACEMENT_3D ( 'NONE', #20889, #7525, #27618 ) ;
#8964=AXIS2_PLACEMENT_3D ( 'NONE', #3517, #17106, #679 ) ;
#8998=FACE_BOUND ( 'NONE', #32392, .T. ) ;
#9022=DIRECTION ( 'NONE',  ( 1.000000000000000000, 0.000000000000000000, 0.000000000000000000 ) ) ;
#9055=EDGE_CURVE ( 'NONE', #30408, #19972, #2228, .T. ) ;
#9083=DIRECTION ( 'NONE',  ( 0.000000000000000000, 0.000000000000000000, -1.000000000000000000 ) ) ;
#9095=FACE_OUTER_BOUND ( 'NONE', #14861, .T. ) ;
#9144=DIRECTION ( 'NONE',  ( 1.000000000000000000, 0.000000000000000000, 0.000000000000000000 ) ) ;
#9224=EDGE_CURVE ( 'NONE', #12270, #5471, #2573, .T. ) ;
#9279=CIRCLE ( 'NONE', #181, 14.99999999999999822 ) ;
#9421=STYLED_ITEM ( 'NONE', ( #37381 ), #13444 ) ;
#9602=CIRCLE ( 'NONE', #39538, 13.40000000000000213 ) ;
#9639=CIRCLE ( 'NONE', #14529, 12.59999999999999964 ) ;
#9643=EDGE_CURVE ( 'NONE', #30408, #27215, #16226, .T. ) ;
#9679=CIRCLE ( 'NONE', #32662, 12.59999999999999964 ) ;
#9705=TOROIDAL_SURFACE ( 'NONE', #37571, 11.08000000000000007, 0.08000000000000020983 ) ;
#9707=EDGE_CURVE ( 'NONE', #30260, #19475, #12765, .T. ) ;
#9801=PRODUCT_CONTEXT ( 'NONE', #767, 'mechanical' ) ;
#9816=CARTESIAN_POINT ( 'NONE',  ( 8.999999999999998224, 1.543054966925665076E-15, 12.59999999999999964 ) ) ;
#9862=CARTESIAN_POINT ( 'NONE',  ( 8.999999999999998224, 0.000000000000000000, 0.000000000000000000 ) ) ;
#9910=CARTESIAN_POINT ( 'NONE',  ( -9.000000000000005329, 14.91999999999999815, 0.000000000000000000 ) ) ;
#9956=DIRECTION ( 'NONE',  ( 0.000000000000000000, 0.000000000000000000, -1.000000000000000000 ) ) ;
#9962=ORIENTED_EDGE ( 'NONE', *, *, #19222, .T. ) ;
#9969=ADVANCED_FACE ( 'NONE', ( #20445 ), #1, .T. ) ;
#9996=DIRECTION ( 'NONE',  ( -1.000000000000000000, -0.000000000000000000, -0.000000000000000000 ) ) ;
#10016=APPLICATION_CONTEXT ( 'automotive_design' ) ;
#10108=AXIS2_PLACEMENT_3D ( 'NONE', #9910, #23259, #36512 ) ;
#10131=CIRCLE ( 'NONE', #24797, 0.08000000000000020983 ) ;
#10158=DIRECTION ( 'NONE',  ( 0.000000000000000000, -1.000000000000000000, 0.000000000000000000 ) ) ;
#10213=DIRECTION ( 'NONE',  ( 1.000000000000000000, 0.000000000000000000, 0.000000000000000000 ) ) ;
#10237=DIRECTION ( 'NONE',  ( 0.000000000000000000, 0.000000000000000000, -1.000000000000000000 ) ) ;
#10431=ORIENTED_EDGE ( 'NONE', *, *, #30528, .F. ) ;
#10461=EDGE_CURVE ( 'NONE', #37611, #30532, #11417, .T. ) ;
#10539=ORIENTED_EDGE ( 'NONE', *, *, #2944, .T. ) ;
#10560=SURFACE_STYLE_USAGE ( .BOTH. , #7268 ) ;
#10755=ADVANCED_FACE ( 'NONE', ( #6548 ), #13794, .T. ) ;
#10809=CARTESIAN_POINT ( 'NONE',  ( -17.77999999999999758, 1.836970198721029589E-15, -14.99999999999999822 ) ) ;
#10951=CIRCLE ( 'NONE', #2527, 11.00000000000000000 ) ;
#10992=ORIENTED_EDGE ( 'NONE', *, *, #19222, .F. ) ;
#11003=CIRCLE ( 'NONE', #37446, 11.08000000000000007 ) ;
#11075=DIRECTION ( 'NONE',  ( 0.000000000000000000, 0.000000000000000000, 1.000000000000000000 ) ) ;
#11128=EDGE_CURVE ( 'NONE', #7493, #35542, #28726, .T. ) ;
#11151=CIRCLE ( 'NONE', #3443, 0.08000000000000020983 ) ;
#11162=DIRECTION ( 'NONE',  ( 0.000000000000000000, 0.000000000000000000, 1.000000000000000000 ) ) ;
#11205=ORIENTED_EDGE ( 'NONE', *, *, #38450, .T. ) ;
#11206=DIRECTION ( 'NONE',  ( 1.000000000000000000, 0.000000000000000000, 0.000000000000000000 ) ) ;
#11209=AXIS2_PLACEMENT_3D ( 'NONE', #30688, #23730, #764 ) ;
#11251=FACE_OUTER_BOUND ( 'NONE', #2273, .T. ) ;
#11311=EDGE_CURVE ( 'NONE', #4861, #39523, #23010, .T. ) ;
#11408=EDGE_LOOP ( 'NONE', ( #33474, #38660, #29524, #28788 ) ) ;
#11417=LINE ( 'NONE', #8345, #32800 ) ;
#11450=AXIS2_PLACEMENT_3D ( 'NONE', #20313, #3876, #10237 ) ;
#11458=CARTESIAN_POINT ( 'NONE',  ( -8.920000000000003482, 0.000000000000000000, 14.99999999999999822 ) ) ;
#11465=ADVANCED_BREP_SHAPE_REPRESENTATION ( '', ( #13444, #13552 ), #41322 ) ;
#11490=DIRECTION ( 'NONE',  ( 0.000000000000000000, 0.000000000000000000, -1.000000000000000000 ) ) ;
#11495=AXIS2_PLACEMENT_3D ( 'NONE', #6204, #42834, #5987 ) ;
#11574=DIRECTION ( 'NONE',  ( 0.000000000000000000, 0.000000000000000000, 1.000000000000000000 ) ) ;
#11575=FACE_BOUND ( 'NONE', #34503, .T. ) ;
#11663=CIRCLE ( 'NONE', #17954, 11.00000000000000000 ) ;
#11823=CARTESIAN_POINT ( 'NONE',  ( -9.000000000000005329, 0.000000000000000000, 0.000000000000000000 ) ) ;
#11831=ORIENTED_EDGE ( 'NONE', *, *, #41699, .T. ) ;
#11852=EDGE_LOOP ( 'NONE', ( #16035, #41873 ) ) ;
#11876=ORIENTED_EDGE ( 'NONE', *, *, #35610, .F. ) ;
#12012=AXIS2_PLACEMENT_3D ( 'NONE', #19069, #16418, #2411 ) ;
#12079=CARTESIAN_POINT ( 'NONE',  ( 9.999999999999998224, 12.59999999999999964, 0.000000000000000000 ) ) ;
#12270=VERTEX_POINT ( 'NONE', #3566 ) ;
#12305=VERTEX_POINT ( 'NONE', #39999 ) ;
#12322=AXIS2_PLACEMENT_3D ( 'NONE', #36043, #14031, #30605 ) ;
#12331=EDGE_CURVE ( 'NONE', #4861, #12270, #970, .T. ) ;
#12391=DIRECTION ( 'NONE',  ( 1.000000000000000000, 0.000000000000000000, 0.000000000000000000 ) ) ;
#12464=EDGE_CURVE ( 'NONE', #35369, #37611, #15654, .T. ) ;
#12602=CARTESIAN_POINT ( 'NONE',  ( 8.999999999999998224, 0.000000000000000000, 0.000000000000000000 ) ) ;
#12649=ORIENTED_EDGE ( 'NONE', *, *, #25986, .T. ) ;
#12730=FACE_OUTER_BOUND ( 'NONE', #31693, .T. ) ;
#12765=CIRCLE ( 'NONE', #5086, 12.59999999999999964 ) ;
#12854=DIRECTION ( 'NONE',  ( -1.000000000000000000, -0.000000000000000000, -0.000000000000000000 ) ) ;
#12866=ADVANCED_FACE ( 'NONE', ( #21845 ), #35093, .T. ) ;
#12883=DIRECTION ( 'NONE',  ( 0.000000000000000000, -1.224646799147343346E-16, 1.000000000000000000 ) ) ;
#12923=FACE_OUTER_BOUND ( 'NONE', #8708, .T. ) ;
#13027=DIRECTION ( 'NONE',  ( 0.000000000000000000, 0.000000000000000000, 1.000000000000000000 ) ) ;
#13044=DIRECTION ( 'NONE',  ( 1.000000000000000000, 0.000000000000000000, 0.000000000000000000 ) ) ;
#13207=EDGE_LOOP ( 'NONE', ( #10431, #32261, #5612, #41555 ) ) ;
#13218=FACE_BOUND ( 'NONE', #35571, .T. ) ;
#13342=EDGE_LOOP ( 'NONE', ( #38691, #3456, #9962, #31334 ) ) ;
#13421=( NAMED_UNIT ( * ) SI_UNIT ( $, .STERADIAN. ) SOLID_ANGLE_UNIT ( ) );
#13444=MANIFOLD_SOLID_BREP ( 'RollersSimplified', #23347 ) ;
#13552=AXIS2_PLACEMENT_3D ( 'NONE', #3852, #14597, #10213 ) ;
#13609=EDGE_LOOP ( 'NONE', ( #25249, #35742, #35688, #41259 ) ) ;
#13738=FACE_OUTER_BOUND ( 'NONE', #13609, .T. ) ;
#13751=ORIENTED_EDGE ( 'NONE', *, *, #17550, .F. ) ;
#13782=VERTEX_POINT ( 'NONE', #21526 ) ;
#13794=CYLINDRICAL_SURFACE ( 'NONE', #32828, 14.99999999999999822 ) ;
#13892=DIRECTION ( 'NONE',  ( 0.000000000000000000, 0.000000000000000000, 1.000000000000000000 ) ) ;
#13946=CARTESIAN_POINT ( 'NONE',  ( -12.69999999999999929, 0.000000000000000000, 0.000000000000000000 ) ) ;
#14001=DIRECTION ( 'NONE',  ( -1.000000000000000000, 0.000000000000000000, -0.000000000000000000 ) ) ;
#14031=DIRECTION ( 'NONE',  ( -1.000000000000000000, -0.000000000000000000, -0.000000000000000000 ) ) ;
#14050=ADVANCED_FACE ( 'NONE', ( #12730 ), #31122, .T. ) ;
#14178=( GEOMETRIC_REPRESENTATION_CONTEXT ( 3 ) GLOBAL_UNCERTAINTY_ASSIGNED_CONTEXT ( ( #20903 ) ) GLOBAL_UNIT_ASSIGNED_CONTEXT ( ( #36294, #29354, #13421 ) ) REPRESENTATION_CONTEXT ( 'NONE', 'WORKASPACE' ) );
#14205=ORIENTED_EDGE ( 'NONE', *, *, #9707, .F. ) ;
#14281=CARTESIAN_POINT ( 'NONE',  ( -8.920000000000003482, 0.000000000000000000, 11.08000000000000007 ) ) ;
#14342=MECHANICAL_DESIGN_GEOMETRIC_PRESENTATION_REPRESENTATION('',(#9421),#19244);
#14402=AXIS2_PLACEMENT_3D ( 'NONE', #817, #4306, #23786 ) ;
#14472=ORIENTED_EDGE ( 'NONE', *, *, #24453, .F. ) ;
#14476=AXIS2_PLACEMENT_3D ( 'NONE', #3089, #16034, #19527 ) ;
#14497=VECTOR ( 'NONE', #31035, 1000.000000000000000 ) ;
#14527=DIRECTION ( 'NONE',  ( 0.000000000000000000, 0.000000000000000000, -1.000000000000000000 ) ) ;
#14529=AXIS2_PLACEMENT_3D ( 'NONE', #8118, #21487, #4846 ) ;
#14597=DIRECTION ( 'NONE',  ( 0.000000000000000000, 0.000000000000000000, 1.000000000000000000 ) ) ;
#14641=CARTESIAN_POINT ( 'NONE',  ( 8.999999999999998224, 0.000000000000000000, 14.91999999999999993 ) ) ;
#14678=AXIS2_PLACEMENT_3D ( 'NONE', #4023, #30676, #13892 ) ;
#14687=ORIENTED_EDGE ( 'NONE', *, *, #9055, .F. ) ;
#14843=AXIS2_PLACEMENT_3D ( 'NONE', #16868, #40148, #24051 ) ;
#14861=EDGE_LOOP ( 'NONE', ( #16143, #19178, #11205, #25313 ) ) ;
#14943=DIRECTION ( 'NONE',  ( 0.000000000000000000, 0.000000000000000000, -1.000000000000000000 ) ) ;
#15009=VERTEX_POINT ( 'NONE', #41085 ) ;
#15194=SHAPE_REPRESENTATION ( 'needle roller bearing_nm_iso_ISO 3030 - 15C2230 - Full,SI,AC,Full', ( #13552 ), #41322 ) ;
#15574=AXIS2_PLACEMENT_3D ( 'NONE', #7761, #4472, #1209 ) ;
#15623=DIRECTION ( 'NONE',  ( 0.000000000000000000, -1.000000000000000000, 0.000000000000000000 ) ) ;
#15654=CIRCLE ( 'NONE', #39984, 13.40000000000000213 ) ;
#15828=PRODUCT_DEFINITION_SHAPE ( 'NONE', 'NONE',  #27627 ) ;
#16034=DIRECTION ( 'NONE',  ( -1.000000000000000000, -0.000000000000000000, -0.000000000000000000 ) ) ;
#16035=ORIENTED_EDGE ( 'NONE', *, *, #36401, .T. ) ;
#16088=CARTESIAN_POINT ( 'NONE',  ( -9.000000000000005329, 0.000000000000000000, 0.000000000000000000 ) ) ;
#16091=EDGE_LOOP ( 'NONE', ( #35619, #28006, #7905, #13751 ) ) ;
#16099=CYLINDRICAL_SURFACE ( 'NONE', #43028, 13.40000000000000213 ) ;
#16138=AXIS2_PLACEMENT_3D ( 'NONE', #8872, #20228, #3369 ) ;
#16143=ORIENTED_EDGE ( 'NONE', *, *, #9643, .F. ) ;
#16190=VECTOR ( 'NONE', #19302, 1000.000000000000000 ) ;
#16226=CIRCLE ( 'NONE', #24595, 0.08000000000000020983 ) ;
#16402=ADVANCED_FACE ( 'NONE', ( #34173 ), #4271, .F. ) ;
#16418=DIRECTION ( 'NONE',  ( -1.000000000000000000, -0.000000000000000000, -0.000000000000000000 ) ) ;
#16432=CARTESIAN_POINT ( 'NONE',  ( -8.920000000000003482, 0.000000000000000000, 0.000000000000000000 ) ) ;
#16484=PRESENTATION_STYLE_ASSIGNMENT (( #29786 ) ) ;
#16485=CYLINDRICAL_SURFACE ( 'NONE', #38543, 11.00000000000000000 ) ;
#16747=EDGE_CURVE ( 'NONE', #30532, #31353, #28307, .T. ) ;
#16764=ORIENTED_EDGE ( 'NONE', *, *, #12331, .T. ) ;
#16868=CARTESIAN_POINT ( 'NONE',  ( 8.919999999999999929, 1.356908653455267209E-15, -11.08000000000000007 ) ) ;
#16940=ORIENTED_EDGE ( 'NONE', *, *, #30810, .F. ) ;
#16966=UNCERTAINTY_MEASURE_WITH_UNIT (LENGTH_MEASURE( 1.000000000000000082E-05 ), #5131, 'distance_accuracy_value', 'NONE');
#16976=FACE_OUTER_BOUND ( 'NONE', #39656, .T. ) ;
#17001=DIRECTION ( 'NONE',  ( 0.000000000000000000, 0.000000000000000000, 1.000000000000000000 ) ) ;
#17042=EDGE_CURVE ( 'NONE', #26006, #12305, #22056, .T. ) ;
#17052=AXIS2_PLACEMENT_3D ( 'NONE', #13946, #27686, #33991 ) ;
#17069=FACE_BOUND ( 'NONE', #27068, .T. ) ;
#17106=DIRECTION ( 'NONE',  ( 1.000000000000000000, 0.000000000000000000, 0.000000000000000000 ) ) ;
#17116=EDGE_LOOP ( 'NONE', ( #7850, #41708, #10539, #31278 ) ) ;
#17152=DIRECTION ( 'NONE',  ( 0.000000000000000000, 0.000000000000000000, 1.000000000000000000 ) ) ;
#17183=VECTOR ( 'NONE', #20933, 1000.000000000000000 ) ;
#17283=ORIENTED_EDGE ( 'NONE', *, *, #1091, .F. ) ;
#17301=CARTESIAN_POINT ( 'NONE',  ( 8.999999999999998224, 14.91999999999999993, 0.000000000000000000 ) ) ;
#17349=EDGE_LOOP ( 'NONE', ( #25763, #27566, #41813, #32460 ) ) ;
#17379=CIRCLE ( 'NONE', #1999, 0.08000000000000020983 ) ;
#17550=EDGE_CURVE ( 'NONE', #39523, #5471, #11663, .T. ) ;
#17703=EDGE_CURVE ( 'NONE', #26433, #19475, #5731, .T. ) ;
#17720=LINE ( 'NONE', #31863, #23069 ) ;
#17770=AXIS2_PLACEMENT_3D ( 'NONE', #5157, #34396, #27440 ) ;
#17772=CARTESIAN_POINT ( 'NONE',  ( -9.000000000000005329, 1.356908653455267209E-15, -11.08000000000000007 ) ) ;
#17838=FACE_OUTER_BOUND ( 'NONE', #25830, .T. ) ;
#17954=AXIS2_PLACEMENT_3D ( 'NONE', #21086, #34551, #30656 ) ;
#17978=EDGE_CURVE ( 'NONE', #18607, #13782, #31187, .T. ) ;
#18068=CARTESIAN_POINT ( 'NONE',  ( -8.920000000000003482, 1.827173024327850982E-15, -14.91999999999999815 ) ) ;
#18156=CYLINDRICAL_SURFACE ( 'NONE', #34055, 13.40000000000000213 ) ;
#18228=AXIS2_PLACEMENT_3D ( 'NONE', #37046, #3215, #6937 ) ;
#18251=ORIENTED_EDGE ( 'NONE', *, *, #30810, .T. ) ;
#18369=EDGE_LOOP ( 'NONE', ( #7461, #10992 ) ) ;
#18479=ORIENTED_EDGE ( 'NONE', *, *, #4397, .T. ) ;
#18584=ORIENTED_EDGE ( 'NONE', *, *, #2944, .F. ) ;
#18605=CARTESIAN_POINT ( 'NONE',  ( 9.999999999999998224, 1.543054966925665076E-15, 12.59999999999999964 ) ) ;
#18607=VERTEX_POINT ( 'NONE', #30967 ) ;
#18767=CIRCLE ( 'NONE', #1285, 14.91999999999999815 ) ;
#18851=ORIENTED_EDGE ( 'NONE', *, *, #22463, .T. ) ;
#18864=CARTESIAN_POINT ( 'NONE',  ( -12.69999999999999929, 1.543054966925665076E-15, 12.59999999999999964 ) ) ;
#18868=FACE_OUTER_BOUND ( 'NONE', #3111, .T. ) ;
#18880=LINE ( 'NONE', #42143, #34220 ) ;
#18950=TOROIDAL_SURFACE ( 'NONE', #21722, 11.08000000000000007, 0.08000000000000020983 ) ;
#19069=CARTESIAN_POINT ( 'NONE',  ( -17.77999999999999758, 0.000000000000000000, 0.000000000000000000 ) ) ;
#19081=STYLED_ITEM ( 'NONE', ( #16484 ), #11465 ) ;
#19178=ORIENTED_EDGE ( 'NONE', *, *, #9055, .T. ) ;
#19222=EDGE_CURVE ( 'NONE', #25155, #5697, #9679, .T. ) ;
#19244=( GEOMETRIC_REPRESENTATION_CONTEXT ( 3 ) GLOBAL_UNCERTAINTY_ASSIGNED_CONTEXT ( ( #32651 ) ) GLOBAL_UNIT_ASSIGNED_CONTEXT ( ( #3756, #40857, #33899 ) ) REPRESENTATION_CONTEXT ( 'NONE', 'WORKASPACE' ) );
#19259=EDGE_LOOP ( 'NONE', ( #17283, #21923 ) ) ;
#19302=DIRECTION ( 'NONE',  ( -1.000000000000000000, -0.000000000000000000, -0.000000000000000000 ) ) ;
#19362=EDGE_CURVE ( 'NONE', #31353, #30532, #22249, .T. ) ;
#19475=VERTEX_POINT ( 'NONE', #6589 ) ;
#19496=ORIENTED_EDGE ( 'NONE', *, *, #38450, .F. ) ;
#19515=CARTESIAN_POINT ( 'NONE',  ( -17.77999999999999758, 1.347111479062088405E-15, -11.00000000000000000 ) ) ;
#19527=DIRECTION ( 'NONE',  ( 0.000000000000000000, 0.000000000000000000, -1.000000000000000000 ) ) ;
#19568=ORIENTED_EDGE ( 'NONE', *, *, #35724, .F. ) ;
#19591=DIRECTION ( 'NONE',  ( 0.000000000000000000, 0.000000000000000000, -1.000000000000000000 ) ) ;
#19650=DIRECTION ( 'NONE',  ( -1.000000000000000000, -0.000000000000000000, -0.000000000000000000 ) ) ;
#19698=CIRCLE ( 'NONE', #3632, 14.91999999999999815 ) ;
#19702=CARTESIAN_POINT ( 'NONE',  ( -9.000000000000005329, 14.91999999999999815, 0.000000000000000000 ) ) ;
#19763=AXIS2_PLACEMENT_3D ( 'NONE', #26995, #29849, #9956 ) ;
#19804=CIRCLE ( 'NONE', #30216, 0.08000000000000020983 ) ;
#19823=ORIENTED_EDGE ( 'NONE', *, *, #20734, .T. ) ;
#19972=VERTEX_POINT ( 'NONE', #14641 ) ;
#20000=CARTESIAN_POINT ( 'NONE',  ( 9.999999999999998224, 0.000000000000000000, 0.000000000000000000 ) ) ;
#20147=CIRCLE ( 'NONE', #7554, 11.00000000000000000 ) ;
#20150=CARTESIAN_POINT ( 'NONE',  ( -9.000000000000005329, 0.000000000000000000, 14.91999999999999815 ) ) ;
#20228=DIRECTION ( 'NONE',  ( -1.000000000000000000, -0.000000000000000000, -0.000000000000000000 ) ) ;
#20313=CARTESIAN_POINT ( 'NONE',  ( -10.00000000000000178, 0.000000000000000000, 0.000000000000000000 ) ) ;
#20419=CARTESIAN_POINT ( 'NONE',  ( -10.00000000000000178, 0.000000000000000000, -12.59999999999999964 ) ) ;
#20438=LINE ( 'NONE', #10809, #22838 ) ;
#20445=FACE_OUTER_BOUND ( 'NONE', #1793, .T. ) ;
#20653=AXIS2_PLACEMENT_3D ( 'NONE', #2064, #15623, #11490 ) ;
#20734=EDGE_CURVE ( 'NONE', #12270, #13782, #17379, .T. ) ;
#20889=CARTESIAN_POINT ( 'NONE',  ( -12.69999999999999929, 0.000000000000000000, 0.000000000000000000 ) ) ;
#20903=UNCERTAINTY_MEASURE_WITH_UNIT (LENGTH_MEASURE( 1.000000000000000082E-05 ), #36294, 'distance_accuracy_value', 'NONE');
#20933=DIRECTION ( 'NONE',  ( 1.000000000000000000, 0.000000000000000000, 0.000000000000000000 ) ) ;
#21009=PLANE ( 'NONE',  #33117 ) ;
#21065=ADVANCED_FACE ( 'NONE', ( #6367 ), #9705, .T. ) ;
#21075=FILL_AREA_STYLE_COLOUR ( '', #33127 ) ;
#21086=CARTESIAN_POINT ( 'NONE',  ( -8.920000000000003482, 0.000000000000000000, 0.000000000000000000 ) ) ;
#21120=CARTESIAN_POINT ( 'NONE',  ( 8.919999999999996376, 0.000000000000000000, 0.000000000000000000 ) ) ;
#21134=DIRECTION ( 'NONE',  ( -1.000000000000000000, -0.000000000000000000, -0.000000000000000000 ) ) ;
#21303=CARTESIAN_POINT ( 'NONE',  ( -10.00000000000000178, 0.000000000000000000, 0.000000000000000000 ) ) ;
#21353=DIRECTION ( 'NONE',  ( -1.000000000000000000, -0.000000000000000000, -0.000000000000000000 ) ) ;
#21367=LINE ( 'NONE', #1881, #8832 ) ;
#21487=DIRECTION ( 'NONE',  ( 1.000000000000000000, 0.000000000000000000, 0.000000000000000000 ) ) ;
#21526=CARTESIAN_POINT ( 'NONE',  ( 8.999999999999998224, 0.000000000000000000, 11.08000000000000007 ) ) ;
#21722=AXIS2_PLACEMENT_3D ( 'NONE', #3441, #19650, #23571 ) ;
#21732=ORIENTED_EDGE ( 'NONE', *, *, #1366, .T. ) ;
#21845=FACE_OUTER_BOUND ( 'NONE', #6883, .T. ) ;
#21923=ORIENTED_EDGE ( 'NONE', *, *, #12464, .F. ) ;
#22056=CIRCLE ( 'NONE', #8772, 13.40000000000000213 ) ;
#22137=FACE_BOUND ( 'NONE', #19259, .T. ) ;
#22249=CIRCLE ( 'NONE', #8964, 13.40000000000000213 ) ;
#22340=DIRECTION ( 'NONE',  ( 1.000000000000000000, 0.000000000000000000, 0.000000000000000000 ) ) ;
#22413=EDGE_LOOP ( 'NONE', ( #2246, #24083 ) ) ;
#22463=EDGE_CURVE ( 'NONE', #5697, #25155, #3764, .T. ) ;
#22797=EDGE_LOOP ( 'NONE', ( #12649, #6287, #32, #8645 ) ) ;
#22805=CARTESIAN_POINT ( 'NONE',  ( 8.919999999999994600, 0.000000000000000000, 0.000000000000000000 ) ) ;
#22838=VECTOR ( 'NONE', #27842, 1000.000000000000000 ) ;
#23010=LINE ( 'NONE', #19515, #16190 ) ;
#23069=VECTOR ( 'NONE', #9144, 1000.000000000000000 ) ;
#23087=DIRECTION ( 'NONE',  ( -1.000000000000000000, -0.000000000000000000, -0.000000000000000000 ) ) ;
#23132=CARTESIAN_POINT ( 'NONE',  ( -17.77999999999999758, 0.000000000000000000, 11.00000000000000000 ) ) ;
#23146=FACE_OUTER_BOUND ( 'NONE', #16091, .T. ) ;
#23158=EDGE_CURVE ( 'NONE', #27215, #40017, #36576, .T. ) ;
#23228=DIRECTION ( 'NONE',  ( 0.000000000000000000, 0.000000000000000000, 1.000000000000000000 ) ) ;
#23259=DIRECTION ( 'NONE',  ( 1.000000000000000000, 0.000000000000000000, 0.000000000000000000 ) ) ;
#23347=CLOSED_SHELL ( 'NONE', ( #36295, #43156, #21065, #26472, #14050, #4998, #41509, #8088, #1088, #29400, #37979, #12866, #36322, #9969, #27858, #10755, #33249, #41398, #41479, #364, #37901, #16402, #40678, #42548, #2107, #30554 ) ) ;
#23381=AXIS2_PLACEMENT_3D ( 'NONE', #21303, #35195, #8580 ) ;
#23484=DIRECTION ( 'NONE',  ( -1.000000000000000000, -0.000000000000000000, -0.000000000000000000 ) ) ;
#23495=VERTEX_POINT ( 'NONE', #8335 ) ;
#23571=DIRECTION ( 'NONE',  ( 0.000000000000000000, 0.000000000000000000, 1.000000000000000000 ) ) ;
#23609=ORIENTED_EDGE ( 'NONE', *, *, #4857, .T. ) ;
#23730=DIRECTION ( 'NONE',  ( -1.000000000000000000, -0.000000000000000000, -0.000000000000000000 ) ) ;
#23778=DIRECTION ( 'NONE',  ( 0.000000000000000000, -1.224646799147343346E-16, 1.000000000000000000 ) ) ;
#23786=DIRECTION ( 'NONE',  ( 0.000000000000000000, 0.000000000000000000, 1.000000000000000000 ) ) ;
#23829=CARTESIAN_POINT ( 'NONE',  ( -17.77999999999999758, 0.000000000000000000, 0.000000000000000000 ) ) ;
#23970=LINE ( 'NONE', #24196, #17183 ) ;
#24041=CARTESIAN_POINT ( 'NONE',  ( 8.999999999999998224, 0.000000000000000000, -13.40000000000000213 ) ) ;
#24051=DIRECTION ( 'NONE',  ( 0.000000000000000000, -1.224646799147343346E-16, 1.000000000000000000 ) ) ;
#24083=ORIENTED_EDGE ( 'NONE', *, *, #27982, .F. ) ;
#24196=CARTESIAN_POINT ( 'NONE',  ( -12.69999999999999929, 0.000000000000000000, -12.59999999999999964 ) ) ;
#24403=DIRECTION ( 'NONE',  ( 0.000000000000000000, 0.000000000000000000, -1.000000000000000000 ) ) ;
#24426=ORIENTED_EDGE ( 'NONE', *, *, #26096, .T. ) ;
#24453=EDGE_CURVE ( 'NONE', #5690, #28933, #36707, .T. ) ;
#24464=CIRCLE ( 'NONE', #11209, 14.91999999999999993 ) ;
#24476=FACE_OUTER_BOUND ( 'NONE', #17349, .T. ) ;
#24595=AXIS2_PLACEMENT_3D ( 'NONE', #28107, #34846, #4959 ) ;
#24599=DIRECTION ( 'NONE',  ( 0.000000000000000000, 0.000000000000000000, 1.000000000000000000 ) ) ;
#24789=DIRECTION ( 'NONE',  ( 1.000000000000000000, 0.000000000000000000, 0.000000000000000000 ) ) ;
#24797=AXIS2_PLACEMENT_3D ( 'NONE', #2800, #32089, #12883 ) ;
#25038=ORIENTED_EDGE ( 'NONE', *, *, #36356, .T. ) ;
#25155=VERTEX_POINT ( 'NONE', #18605 ) ;
#25164=AXIS2_PLACEMENT_3D ( 'NONE', #6726, #9996, #30096 ) ;
#25249=ORIENTED_EDGE ( 'NONE', *, *, #17703, .F. ) ;
#25313=ORIENTED_EDGE ( 'NONE', *, *, #23158, .F. ) ;
#25397=PLANE ( 'NONE',  #37071 ) ;
#25763=ORIENTED_EDGE ( 'NONE', *, *, #1091, .T. ) ;
#25822=CARTESIAN_POINT ( 'NONE',  ( -8.920000000000003482, 1.836970198721029589E-15, -14.99999999999999822 ) ) ;
#25830=EDGE_LOOP ( 'NONE', ( #23609, #4567, #42760, #19496 ) ) ;
#25920=DIRECTION ( 'NONE',  ( 0.000000000000000000, 0.000000000000000000, 1.000000000000000000 ) ) ;
#25986=EDGE_CURVE ( 'NONE', #35289, #5690, #9279, .T. ) ;
#26006=VERTEX_POINT ( 'NONE', #4259 ) ;
#26077=( NAMED_UNIT ( * ) SI_UNIT ( $, .STERADIAN. ) SOLID_ANGLE_UNIT ( ) );
#26089=ORIENTED_EDGE ( 'NONE', *, *, #37709, .F. ) ;
#26096=EDGE_CURVE ( 'NONE', #40017, #27215, #34354, .T. ) ;
#26230=AXIS2_PLACEMENT_3D ( 'NONE', #12079, #5513, #6148 ) ;
#26269=DIRECTION ( 'NONE',  ( -1.000000000000000000, -0.000000000000000000, -0.000000000000000000 ) ) ;
#26429=ORIENTED_EDGE ( 'NONE', *, *, #1366, .F. ) ;
#26433=VERTEX_POINT ( 'NONE', #27760 ) ;
#26443=DIRECTION ( 'NONE',  ( 0.000000000000000000, 0.000000000000000000, -1.000000000000000000 ) ) ;
#26472=ADVANCED_FACE ( 'NONE', ( #872 ), #16485, .F. ) ;
#26476=LINE ( 'NONE', #41261, #14497 ) ;
#26509=FACE_OUTER_BOUND ( 'NONE', #11852, .T. ) ;
#26586=CARTESIAN_POINT ( 'NONE',  ( -8.920000000000003482, 0.000000000000000000, 0.000000000000000000 ) ) ;
#26689=DIRECTION ( 'NONE',  ( -1.000000000000000000, -0.000000000000000000, -0.000000000000000000 ) ) ;
#26691=ORIENTED_EDGE ( 'NONE', *, *, #41699, .F. ) ;
#26723=DIRECTION ( 'NONE',  ( 1.000000000000000000, 0.000000000000000000, 0.000000000000000000 ) ) ;
#26869=EDGE_CURVE ( 'NONE', #27839, #26433, #32997, .T. ) ;
#26941=AXIS2_PLACEMENT_3D ( 'NONE', #35695, #42030, #32028 ) ;
#26995=CARTESIAN_POINT ( 'NONE',  ( -12.69999999999999929, 0.000000000000000000, 0.000000000000000000 ) ) ;
#27054=ORIENTED_EDGE ( 'NONE', *, *, #4857, .F. ) ;
#27068=EDGE_LOOP ( 'NONE', ( #18479, #35122 ) ) ;
#27132=CARTESIAN_POINT ( 'NONE',  ( -9.000000000000007105, 0.000000000000000000, 0.000000000000000000 ) ) ;
#27138=VERTEX_POINT ( 'NONE', #39626 ) ;
#27206=AXIS2_PLACEMENT_3D ( 'NONE', #4585, #31444, #30794 ) ;
#27215=VERTEX_POINT ( 'NONE', #32243 ) ;
#27259=ORIENTED_EDGE ( 'NONE', *, *, #4397, .F. ) ;
#27270=AXIS2_PLACEMENT_3D ( 'NONE', #21120, #37637, #24599 ) ;
#27407=CARTESIAN_POINT ( 'NONE',  ( -12.69999999999999929, 1.641026710857453510E-15, 13.40000000000000213 ) ) ;
#27440=DIRECTION ( 'NONE',  ( 0.000000000000000000, 0.000000000000000000, -1.000000000000000000 ) ) ;
#27452=CYLINDRICAL_SURFACE ( 'NONE', #17052, 12.59999999999999964 ) ;
#27548=ORIENTED_EDGE ( 'NONE', *, *, #9224, .F. ) ;
#27566=ORIENTED_EDGE ( 'NONE', *, *, #37709, .T. ) ;
#27584=ORIENTED_EDGE ( 'NONE', *, *, #19362, .T. ) ;
#27618=DIRECTION ( 'NONE',  ( 0.000000000000000000, 0.000000000000000000, -1.000000000000000000 ) ) ;
#27627=PRODUCT_DEFINITION ( 'UNKNOWN', '', #34420, #760 ) ;
#27686=DIRECTION ( 'NONE',  ( 1.000000000000000000, 0.000000000000000000, 0.000000000000000000 ) ) ;
#27710=CIRCLE ( 'NONE', #14476, 13.40000000000000213 ) ;
#27730=AXIS2_PLACEMENT_3D ( 'NONE', #32364, #29324, #35207 ) ;
#27760=CARTESIAN_POINT ( 'NONE',  ( -10.00000000000000178, 1.543054966925665076E-15, 12.59999999999999964 ) ) ;
#27839=VERTEX_POINT ( 'NONE', #20419 ) ;
#27842=DIRECTION ( 'NONE',  ( -1.000000000000000000, -0.000000000000000000, -0.000000000000000000 ) ) ;
#27853=DIRECTION ( 'NONE',  ( -0.000000000000000000, 1.000000000000000000, 1.224646799147353207E-16 ) ) ;
#27858=ADVANCED_FACE ( 'NONE', ( #13218, #26509 ), #39783, .F. ) ;
#27952=CARTESIAN_POINT ( 'NONE',  ( -10.00000000000000178, 13.40000000000000036, 0.000000000000000000 ) ) ;
#27982=EDGE_CURVE ( 'NONE', #15009, #23495, #5262, .T. ) ;
#28006=ORIENTED_EDGE ( 'NONE', *, *, #5908, .T. ) ;
#28049=CYLINDRICAL_SURFACE ( 'NONE', #43018, 12.59999999999999964 ) ;
#28075=CIRCLE ( 'NONE', #14843, 0.08000000000000020983 ) ;
#28107=CARTESIAN_POINT ( 'NONE',  ( 8.919999999999996376, 1.827173024327850982E-15, -14.91999999999999815 ) ) ;
#28162=CARTESIAN_POINT ( 'NONE',  ( 9.999999999999998224, 1.641026710857453510E-15, 13.40000000000000213 ) ) ;
#28242=ORIENTED_EDGE ( 'NONE', *, *, #11311, .T. ) ;
#28307=CIRCLE ( 'NONE', #31774, 13.40000000000000213 ) ;
#28726=CIRCLE ( 'NONE', #38430, 12.59999999999999964 ) ;
#28742=EDGE_CURVE ( 'NONE', #5471, #39523, #10951, .T. ) ;
#28788=ORIENTED_EDGE ( 'NONE', *, *, #6810, .F. ) ;
#28859=ORIENTED_EDGE ( 'NONE', *, *, #4256, .F. ) ;
#28933=VERTEX_POINT ( 'NONE', #29812 ) ;
#29178=CARTESIAN_POINT ( 'NONE',  ( 8.999999999999998224, 1.832071611524440088E-15, -14.91999999999999993 ) ) ;
#29180=DIRECTION ( 'NONE',  ( 0.000000000000000000, 0.000000000000000000, -1.000000000000000000 ) ) ;
#29212=ORIENTED_EDGE ( 'NONE', *, *, #41815, .F. ) ;
#29304=DIRECTION ( 'NONE',  ( 1.000000000000000000, 0.000000000000000000, 0.000000000000000000 ) ) ;
#29313=DIRECTION ( 'NONE',  ( 1.000000000000000000, 0.000000000000000000, 0.000000000000000000 ) ) ;
#29324=DIRECTION ( 'NONE',  ( 1.000000000000000000, 0.000000000000000000, 0.000000000000000000 ) ) ;
#29354=( NAMED_UNIT ( * ) PLANE_ANGLE_UNIT ( ) SI_UNIT ( $, .RADIAN. ) );
#29400=ADVANCED_FACE ( 'NONE', ( #1177 ), #28049, .F. ) ;
#29524=ORIENTED_EDGE ( 'NONE', *, *, #28742, .F. ) ;
#29563=AXIS2_PLACEMENT_3D ( 'NONE', #40226, #23484, #17152 ) ;
#29786=SURFACE_STYLE_USAGE ( .BOTH. , #53 ) ;
#29812=CARTESIAN_POINT ( 'NONE',  ( -9.000000000000005329, 1.832071611524440088E-15, -14.91999999999999815 ) ) ;
#29849=DIRECTION ( 'NONE',  ( 1.000000000000000000, 0.000000000000000000, 0.000000000000000000 ) ) ;
#30002=SURFACE_STYLE_FILL_AREA ( #3112 ) ;
#30046=LINE ( 'NONE', #27407, #4031 ) ;
#30049=CARTESIAN_POINT ( 'NONE',  ( 8.919999999999998153, 1.352010066258677905E-15, -11.00000000000000000 ) ) ;
#30096=DIRECTION ( 'NONE',  ( 0.000000000000000000, 0.000000000000000000, 1.000000000000000000 ) ) ;
#30205=( NAMED_UNIT ( * ) PLANE_ANGLE_UNIT ( ) SI_UNIT ( $, .RADIAN. ) );
#30216=AXIS2_PLACEMENT_3D ( 'NONE', #14281, #31294, #14943 ) ;
#30259=CYLINDRICAL_SURFACE ( 'NONE', #19763, 12.59999999999999964 ) ;
#30260=VERTEX_POINT ( 'NONE', #2091 ) ;
#30354=DIRECTION ( 'NONE',  ( -0.000000000000000000, 0.000000000000000000, 1.000000000000000000 ) ) ;
#30408=VERTEX_POINT ( 'NONE', #29178 ) ;
#30528=EDGE_CURVE ( 'NONE', #27215, #5690, #20438, .T. ) ;
#30532=VERTEX_POINT ( 'NONE', #41095 ) ;
#30554=ADVANCED_FACE ( 'NONE', ( #11251 ), #37406, .T. ) ;
#30588=AXIS2_PLACEMENT_3D ( 'NONE', #27952, #850, #30983 ) ;
#30596=ORIENTED_EDGE ( 'NONE', *, *, #36356, .F. ) ;
#30599=EDGE_LOOP ( 'NONE', ( #14205, #18584 ) ) ;
#30605=DIRECTION ( 'NONE',  ( 0.000000000000000000, 0.000000000000000000, 1.000000000000000000 ) ) ;
#30626=ORIENTED_EDGE ( 'NONE', *, *, #12464, .T. ) ;
#30656=DIRECTION ( 'NONE',  ( 0.000000000000000000, 0.000000000000000000, 1.000000000000000000 ) ) ;
#30676=DIRECTION ( 'NONE',  ( -1.000000000000000000, -0.000000000000000000, -0.000000000000000000 ) ) ;
#30688=CARTESIAN_POINT ( 'NONE',  ( 8.999999999999998224, 0.000000000000000000, 0.000000000000000000 ) ) ;
#30756=TOROIDAL_SURFACE ( 'NONE', #27270, 14.91999999999999815, 0.08000000000000020983 ) ;
#30794=DIRECTION ( 'NONE',  ( 0.000000000000000000, 0.000000000000000000, 1.000000000000000000 ) ) ;
#30810=EDGE_CURVE ( 'NONE', #12305, #26006, #27710, .T. ) ;
#30967=CARTESIAN_POINT ( 'NONE',  ( 8.999999999999998224, 1.356908653455267209E-15, -11.08000000000000007 ) ) ;
#30983=DIRECTION ( 'NONE',  ( -0.000000000000000000, 0.000000000000000000, 1.000000000000000000 ) ) ;
#31020=AXIS2_PLACEMENT_3D ( 'NONE', #4997, #8278, #41853 ) ;
#31035=DIRECTION ( 'NONE',  ( 1.000000000000000000, 0.000000000000000000, 0.000000000000000000 ) ) ;
#31042=ORIENTED_EDGE ( 'NONE', *, *, #11128, .F. ) ;
#31122=TOROIDAL_SURFACE ( 'NONE', #12322, 11.08000000000000007, 0.07999999999999934941 ) ;
#31144=CARTESIAN_POINT ( 'NONE',  ( -8.920000000000003482, 0.000000000000000000, 0.000000000000000000 ) ) ;
#31187=CIRCLE ( 'NONE', #36036, 11.08000000000000007 ) ;
#31278=ORIENTED_EDGE ( 'NONE', *, *, #6991, .F. ) ;
#31289=SURFACE_STYLE_FILL_AREA ( #41068 ) ;
#31294=DIRECTION ( 'NONE',  ( 0.000000000000000000, -1.000000000000000000, 0.000000000000000000 ) ) ;
#31306=EDGE_LOOP ( 'NONE', ( #26691, #16764, #19823, #36042 ) ) ;
#31334=ORIENTED_EDGE ( 'NONE', *, *, #34598, .F. ) ;
#31353=VERTEX_POINT ( 'NONE', #28162 ) ;
#31428=AXIS2_PLACEMENT_3D ( 'NONE', #26586, #3629, #17001 ) ;
#31444=DIRECTION ( 'NONE',  ( -1.000000000000000000, -0.000000000000000000, -0.000000000000000000 ) ) ;
#31693=EDGE_LOOP ( 'NONE', ( #25038, #11831, #27259, #5385 ) ) ;
#31774=AXIS2_PLACEMENT_3D ( 'NONE', #20000, #26723, #36306 ) ;
#31863=CARTESIAN_POINT ( 'NONE',  ( -12.69999999999999929, 1.641026710857453510E-15, 13.40000000000000213 ) ) ;
#32028=DIRECTION ( 'NONE',  ( 0.000000000000000000, 0.000000000000000000, 1.000000000000000000 ) ) ;
#32089=DIRECTION ( 'NONE',  ( -0.000000000000000000, 1.000000000000000000, 1.224646799147353207E-16 ) ) ;
#32225=DIRECTION ( 'NONE',  ( 0.000000000000000000, 0.000000000000000000, 1.000000000000000000 ) ) ;
#32243=CARTESIAN_POINT ( 'NONE',  ( 8.919999999999994600, 1.836970198721029589E-15, -14.99999999999999822 ) ) ;
#32261=ORIENTED_EDGE ( 'NONE', *, *, #23158, .T. ) ;
#32343=ORIENTED_EDGE ( 'NONE', *, *, #27982, .T. ) ;
#32352=CARTESIAN_POINT ( 'NONE',  ( -12.69999999999999929, 1.543054966925665076E-15, 12.59999999999999964 ) ) ;
#32364=CARTESIAN_POINT ( 'NONE',  ( -10.00000000000000178, 0.000000000000000000, 0.000000000000000000 ) ) ;
#32392=EDGE_LOOP ( 'NONE', ( #11876, #4428 ) ) ;
#32460=ORIENTED_EDGE ( 'NONE', *, *, #10461, .F. ) ;
#32545=CARTESIAN_POINT ( 'NONE',  ( 8.919999999999994600, 0.000000000000000000, 14.99999999999999822 ) ) ;
#32596=CIRCLE ( 'NONE', #27730, 13.40000000000000036 ) ;
#32651=UNCERTAINTY_MEASURE_WITH_UNIT (LENGTH_MEASURE( 1.000000000000000082E-05 ), #3756, 'distance_accuracy_value', 'NONE');
#32662=AXIS2_PLACEMENT_3D ( 'NONE', #5326, #9022, #39107 ) ;
#32800=VECTOR ( 'NONE', #11206, 1000.000000000000000 ) ;
#32828=AXIS2_PLACEMENT_3D ( 'NONE', #23829, #34413, #36224 ) ;
#32967=DIRECTION ( 'NONE',  ( 1.000000000000000000, 0.000000000000000000, 0.000000000000000000 ) ) ;
#32997=CIRCLE ( 'NONE', #11450, 12.59999999999999964 ) ;
#33066=ORIENTED_EDGE ( 'NONE', *, *, #16747, .T. ) ;
#33117=AXIS2_PLACEMENT_3D ( 'NONE', #17301, #14001, #30354 ) ;
#33127=COLOUR_RGB ( '', 0.66274510, 0.83137255, 0.94901961) ;
#33138=ORIENTED_EDGE ( 'NONE', *, *, #9224, .T. ) ;
#33249=ADVANCED_FACE ( 'NONE', ( #9095 ), #7429, .T. ) ;
#33289=DIRECTION ( 'NONE',  ( 0.000000000000000000, -1.000000000000000000, 0.000000000000000000 ) ) ;
#33308=CARTESIAN_POINT ( 'NONE',  ( -8.920000000000003482, 0.000000000000000000, 0.000000000000000000 ) ) ;
#33419=DIRECTION ( 'NONE',  ( -1.000000000000000000, -0.000000000000000000, -0.000000000000000000 ) ) ;
#33474=ORIENTED_EDGE ( 'NONE', *, *, #35610, .T. ) ;
#33586=ORIENTED_EDGE ( 'NONE', *, *, #26869, .T. ) ;
#33617=CARTESIAN_POINT ( 'NONE',  ( 9.999999999999998224, 0.000000000000000000, -12.59999999999999964 ) ) ;
#33816=DIRECTION ( 'NONE',  ( -1.000000000000000000, -0.000000000000000000, -0.000000000000000000 ) ) ;
#33899=( NAMED_UNIT ( * ) SI_UNIT ( $, .STERADIAN. ) SOLID_ANGLE_UNIT ( ) );
#33991=DIRECTION ( 'NONE',  ( 0.000000000000000000, 0.000000000000000000, -1.000000000000000000 ) ) ;
#34055=AXIS2_PLACEMENT_3D ( 'NONE', #1509, #4341, #7631 ) ;
#34173=FACE_OUTER_BOUND ( 'NONE', #7913, .T. ) ;
#34220=VECTOR ( 'NONE', #29304, 1000.000000000000000 ) ;
#34354=CIRCLE ( 'NONE', #15574, 14.99999999999999822 ) ;
#34396=DIRECTION ( 'NONE',  ( 1.000000000000000000, 0.000000000000000000, 0.000000000000000000 ) ) ;
#34413=DIRECTION ( 'NONE',  ( -1.000000000000000000, -0.000000000000000000, -0.000000000000000000 ) ) ;
#34420=PRODUCT_DEFINITION_FORMATION_WITH_SPECIFIED_SOURCE ( 'ANY', '', #113, .NOT_KNOWN. ) ;
#34503=EDGE_LOOP ( 'NONE', ( #33586, #8572 ) ) ;
#34551=DIRECTION ( 'NONE',  ( -1.000000000000000000, -0.000000000000000000, -0.000000000000000000 ) ) ;
#34579=CARTESIAN_POINT ( 'NONE',  ( -8.920000000000003482, 1.347111479062088405E-15, -11.00000000000000000 ) ) ;
#34598=EDGE_CURVE ( 'NONE', #35542, #5697, #23970, .T. ) ;
#34788=CARTESIAN_POINT ( 'NONE',  ( 8.999999999999998224, 1.641026710857453510E-15, 13.40000000000000213 ) ) ;
#34846=DIRECTION ( 'NONE',  ( -0.000000000000000000, 1.000000000000000000, 1.224646799147353207E-16 ) ) ;
#34877=EDGE_CURVE ( 'NONE', #40017, #35289, #21367, .T. ) ;
#35093=CYLINDRICAL_SURFACE ( 'NONE', #31020, 13.40000000000000213 ) ;
#35122=ORIENTED_EDGE ( 'NONE', *, *, #17978, .T. ) ;
#35195=DIRECTION ( 'NONE',  ( 1.000000000000000000, 0.000000000000000000, 0.000000000000000000 ) ) ;
#35207=DIRECTION ( 'NONE',  ( 0.000000000000000000, 0.000000000000000000, -1.000000000000000000 ) ) ;
#35243=CIRCLE ( 'NONE', #20653, 0.08000000000000020983 ) ;
#35289=VERTEX_POINT ( 'NONE', #11458 ) ;
#35369=VERTEX_POINT ( 'NONE', #34788 ) ;
#35396=DIRECTION ( 'NONE',  ( -0.000000000000000000, 0.000000000000000000, 1.000000000000000000 ) ) ;
#35440=EDGE_CURVE ( 'NONE', #23495, #15009, #32596, .T. ) ;
#35542=VERTEX_POINT ( 'NONE', #42163 ) ;
#35571=EDGE_LOOP ( 'NONE', ( #16940, #38645 ) ) ;
#35594=PLANE ( 'NONE',  #6393 ) ;
#35610=EDGE_CURVE ( 'NONE', #27138, #37158, #11003, .T. ) ;
#35619=ORIENTED_EDGE ( 'NONE', *, *, #3974, .F. ) ;
#35688=ORIENTED_EDGE ( 'NONE', *, *, #6991, .T. ) ;
#35695=CARTESIAN_POINT ( 'NONE',  ( 8.919999999999996376, 0.000000000000000000, 0.000000000000000000 ) ) ;
#35724=EDGE_CURVE ( 'NONE', #23495, #12305, #26476, .T. ) ;
#35742=ORIENTED_EDGE ( 'NONE', *, *, #26869, .F. ) ;
#35770=EDGE_CURVE ( 'NONE', #26433, #27839, #9639, .T. ) ;
#35966=EDGE_CURVE ( 'NONE', #5690, #35289, #5443, .T. ) ;
#35999=CARTESIAN_POINT ( 'NONE',  ( -8.920000000000003482, 0.000000000000000000, 0.000000000000000000 ) ) ;
#36036=AXIS2_PLACEMENT_3D ( 'NONE', #9862, #461, #40385 ) ;
#36042=ORIENTED_EDGE ( 'NONE', *, *, #17978, .F. ) ;
#36043=CARTESIAN_POINT ( 'NONE',  ( 8.919999999999999929, 0.000000000000000000, 0.000000000000000000 ) ) ;
#36098=AXIS2_PLACEMENT_3D ( 'NONE', #35999, #38422, #2393 ) ;
#36224=DIRECTION ( 'NONE',  ( 0.000000000000000000, 0.000000000000000000, 1.000000000000000000 ) ) ;
#36294=( LENGTH_UNIT ( ) NAMED_UNIT ( * ) SI_UNIT ( .MILLI., .METRE. ) );
#36295=ADVANCED_FACE ( 'NONE', ( #24476 ), #18156, .T. ) ;
#36306=DIRECTION ( 'NONE',  ( 0.000000000000000000, 0.000000000000000000, -1.000000000000000000 ) ) ;
#36322=ADVANCED_FACE ( 'NONE', ( #11575, #40558 ), #41208, .T. ) ;
#36338=CARTESIAN_POINT ( 'NONE',  ( -12.69999999999999929, 0.000000000000000000, 0.000000000000000000 ) ) ;
#36351=ORIENTED_EDGE ( 'NONE', *, *, #35966, .T. ) ;
#36356=EDGE_CURVE ( 'NONE', #12270, #4861, #20147, .T. ) ;
#36401=EDGE_CURVE ( 'NONE', #2262, #28933, #18767, .T. ) ;
#36512=DIRECTION ( 'NONE',  ( 0.000000000000000000, 0.000000000000000000, -1.000000000000000000 ) ) ;
#36576=CIRCLE ( 'NONE', #8723, 14.99999999999999822 ) ;
#36707=CIRCLE ( 'NONE', #8066, 0.08000000000000020983 ) ;
#36740=EDGE_LOOP ( 'NONE', ( #37881, #28242, #39442, #27548 ) ) ;
#36759=AXIS2_PLACEMENT_3D ( 'NONE', #37654, #21134, #11075 ) ;
#36827=FACE_OUTER_BOUND ( 'NONE', #13342, .T. ) ;
#37046=CARTESIAN_POINT ( 'NONE',  ( -12.69999999999999929, 0.000000000000000000, 0.000000000000000000 ) ) ;
#37071=AXIS2_PLACEMENT_3D ( 'NONE', #38653, #8778, #35396 ) ;
#37158=VERTEX_POINT ( 'NONE', #17772 ) ;
#37354=CIRCLE ( 'NONE', #14402, 11.08000000000000007 ) ;
#37381=PRESENTATION_STYLE_ASSIGNMENT (( #10560 ) ) ;
#37406=CYLINDRICAL_SURFACE ( 'NONE', #8878, 13.40000000000000213 ) ;
#37446=AXIS2_PLACEMENT_3D ( 'NONE', #27132, #26689, #23228 ) ;
#37571=AXIS2_PLACEMENT_3D ( 'NONE', #16432, #33419, #3288 ) ;
#37611=VERTEX_POINT ( 'NONE', #24041 ) ;
#37637=DIRECTION ( 'NONE',  ( -1.000000000000000000, -0.000000000000000000, -0.000000000000000000 ) ) ;
#37654=CARTESIAN_POINT ( 'NONE',  ( -17.77999999999999758, 0.000000000000000000, 0.000000000000000000 ) ) ;
#37668=DIRECTION ( 'NONE',  ( -1.000000000000000000, -0.000000000000000000, -0.000000000000000000 ) ) ;
#37695=EDGE_LOOP ( 'NONE', ( #7802, #31042 ) ) ;
#37709=EDGE_CURVE ( 'NONE', #35369, #31353, #17720, .T. ) ;
#37819=CARTESIAN_POINT ( 'NONE',  ( 8.999999999999998224, 0.000000000000000000, 0.000000000000000000 ) ) ;
#37881=ORIENTED_EDGE ( 'NONE', *, *, #12331, .F. ) ;
#37901=ADVANCED_FACE ( 'NONE', ( #6499 ), #705, .T. ) ;
#37979=ADVANCED_FACE ( 'NONE', ( #13738 ), #39445, .F. ) ;
#38422=DIRECTION ( 'NONE',  ( -1.000000000000000000, -0.000000000000000000, -0.000000000000000000 ) ) ;
#38430=AXIS2_PLACEMENT_3D ( 'NONE', #39611, #23087, #32225 ) ;
#38441=FACE_OUTER_BOUND ( 'NONE', #8726, .T. ) ;
#38450=EDGE_CURVE ( 'NONE', #19972, #40017, #11151, .T. ) ;
#38463=DIRECTION ( 'NONE',  ( 0.000000000000000000, 0.000000000000000000, 1.000000000000000000 ) ) ;
#38543=AXIS2_PLACEMENT_3D ( 'NONE', #40373, #3929, #7442 ) ;
#38645=ORIENTED_EDGE ( 'NONE', *, *, #17042, .F. ) ;
#38653=CARTESIAN_POINT ( 'NONE',  ( 8.999999999999998224, 14.91999999999999993, 0.000000000000000000 ) ) ;
#38660=ORIENTED_EDGE ( 'NONE', *, *, #3974, .T. ) ;
#38691=ORIENTED_EDGE ( 'NONE', *, *, #8418, .T. ) ;
#38870=LINE ( 'NONE', #18864, #1820 ) ;
#39107=DIRECTION ( 'NONE',  ( 0.000000000000000000, 0.000000000000000000, -1.000000000000000000 ) ) ;
#39229=COLOUR_RGB ( '', 0.66274510, 0.83137255, 0.94901961) ;
#39341=SHAPE_REPRESENTATION_RELATIONSHIP ( 'NONE' , 'NONE' ,  #15194, #11465 ) ;
#39442=ORIENTED_EDGE ( 'NONE', *, *, #17550, .T. ) ;
#39445=CYLINDRICAL_SURFACE ( 'NONE', #18228, 12.59999999999999964 ) ;
#39523=VERTEX_POINT ( 'NONE', #34579 ) ;
#39538=AXIS2_PLACEMENT_3D ( 'NONE', #12602, #13044, #25920 ) ;
#39611=CARTESIAN_POINT ( 'NONE',  ( 8.999999999999998224, 0.000000000000000000, 0.000000000000000000 ) ) ;
#39626=CARTESIAN_POINT ( 'NONE',  ( -9.000000000000005329, 0.000000000000000000, 11.08000000000000007 ) ) ;
#39656=EDGE_LOOP ( 'NONE', ( #28859, #40951, #42947, #18851 ) ) ;
#39673=ORIENTED_EDGE ( 'NONE', *, *, #30528, .T. ) ;
#39783=PLANE ( 'NONE',  #10108 ) ;
#39850=VECTOR ( 'NONE', #12854, 1000.000000000000000 ) ;
#39984=AXIS2_PLACEMENT_3D ( 'NONE', #37819, #40872, #38463 ) ;
#39999=CARTESIAN_POINT ( 'NONE',  ( -9.000000000000005329, 0.000000000000000000, -13.40000000000000213 ) ) ;
#40017=VERTEX_POINT ( 'NONE', #32545 ) ;
#40148=DIRECTION ( 'NONE',  ( -0.000000000000000000, 1.000000000000000000, 1.224646799147353207E-16 ) ) ;
#40226=CARTESIAN_POINT ( 'NONE',  ( 8.919999999999998153, 0.000000000000000000, 0.000000000000000000 ) ) ;
#40373=CARTESIAN_POINT ( 'NONE',  ( -17.77999999999999758, 0.000000000000000000, 0.000000000000000000 ) ) ;
#40385=DIRECTION ( 'NONE',  ( 0.000000000000000000, 0.000000000000000000, 1.000000000000000000 ) ) ;
#40474=DIRECTION ( 'NONE',  ( 0.000000000000000000, 0.000000000000000000, 1.000000000000000000 ) ) ;
#40558=FACE_OUTER_BOUND ( 'NONE', #22413, .T. ) ;
#40676=DIRECTION ( 'NONE',  ( 1.000000000000000000, 0.000000000000000000, 0.000000000000000000 ) ) ;
#40678=ADVANCED_FACE ( 'NONE', ( #23146 ), #18950, .T. ) ;
#40857=( NAMED_UNIT ( * ) PLANE_ANGLE_UNIT ( ) SI_UNIT ( $, .RADIAN. ) );
#40872=DIRECTION ( 'NONE',  ( 1.000000000000000000, 0.000000000000000000, 0.000000000000000000 ) ) ;
#40951=ORIENTED_EDGE ( 'NONE', *, *, #11128, .T. ) ;
#41015=DIRECTION ( 'NONE',  ( -1.000000000000000000, -0.000000000000000000, -0.000000000000000000 ) ) ;
#41068=FILL_AREA_STYLE ('',( #21075 ) ) ;
#41085=CARTESIAN_POINT ( 'NONE',  ( -10.00000000000000178, 1.641026710857453312E-15, 13.40000000000000036 ) ) ;
#41095=CARTESIAN_POINT ( 'NONE',  ( 9.999999999999998224, 0.000000000000000000, -13.40000000000000213 ) ) ;
#41208=PLANE ( 'NONE',  #30588 ) ;
#41259=ORIENTED_EDGE ( 'NONE', *, *, #9707, .T. ) ;
#41261=CARTESIAN_POINT ( 'NONE',  ( -12.69999999999999929, 0.000000000000000000, -13.40000000000000213 ) ) ;
#41299=ORIENTED_EDGE ( 'NONE', *, *, #11311, .F. ) ;
#41308=CARTESIAN_POINT ( 'NONE',  ( -12.69999999999999929, 0.000000000000000000, 0.000000000000000000 ) ) ;
#41322=( GEOMETRIC_REPRESENTATION_CONTEXT ( 3 ) GLOBAL_UNCERTAINTY_ASSIGNED_CONTEXT ( ( #16966 ) ) GLOBAL_UNIT_ASSIGNED_CONTEXT ( ( #5131, #30205, #26077 ) ) REPRESENTATION_CONTEXT ( 'NONE', 'WORKASPACE' ) );
#41398=ADVANCED_FACE ( 'NONE', ( #22137, #38441 ), #25397, .F. ) ;
#41418=CIRCLE ( 'NONE', #11495, 12.59999999999999964 ) ;
#41479=ADVANCED_FACE ( 'NONE', ( #5920, #8998 ), #35594, .F. ) ;
#41505=CARTESIAN_POINT ( 'NONE',  ( -8.920000000000003482, 0.000000000000000000, 11.00000000000000000 ) ) ;
#41509=ADVANCED_FACE ( 'NONE', ( #12923 ), #3046, .T. ) ;
#41555=ORIENTED_EDGE ( 'NONE', *, *, #35966, .F. ) ;
#41699=EDGE_CURVE ( 'NONE', #4861, #18607, #28075, .T. ) ;
#41708=ORIENTED_EDGE ( 'NONE', *, *, #17703, .T. ) ;
#41813=ORIENTED_EDGE ( 'NONE', *, *, #16747, .F. ) ;
#41815=EDGE_CURVE ( 'NONE', #28933, #2262, #19698, .T. ) ;
#41853=DIRECTION ( 'NONE',  ( 0.000000000000000000, 0.000000000000000000, -1.000000000000000000 ) ) ;
#41873=ORIENTED_EDGE ( 'NONE', *, *, #41815, .T. ) ;
#42030=DIRECTION ( 'NONE',  ( -1.000000000000000000, -0.000000000000000000, -0.000000000000000000 ) ) ;
#42143=CARTESIAN_POINT ( 'NONE',  ( -12.69999999999999929, 0.000000000000000000, -12.59999999999999964 ) ) ;
#42163=CARTESIAN_POINT ( 'NONE',  ( 8.999999999999998224, 0.000000000000000000, -12.59999999999999964 ) ) ;
#42462=DIRECTION ( 'NONE',  ( 0.000000000000000000, 0.000000000000000000, -1.000000000000000000 ) ) ;
#42548=ADVANCED_FACE ( 'NONE', ( #16976 ), #30259, .F. ) ;
#42760=ORIENTED_EDGE ( 'NONE', *, *, #26096, .F. ) ;
#42834=DIRECTION ( 'NONE',  ( 1.000000000000000000, 0.000000000000000000, 0.000000000000000000 ) ) ;
#42870=DIRECTION ( 'NONE',  ( -1.000000000000000000, -0.000000000000000000, -0.000000000000000000 ) ) ;
#42882=FACE_OUTER_BOUND ( 'NONE', #2921, .T. ) ;
#42947=ORIENTED_EDGE ( 'NONE', *, *, #34598, .T. ) ;
#43018=AXIS2_PLACEMENT_3D ( 'NONE', #41308, #24789, #14527 ) ;
#43028=AXIS2_PLACEMENT_3D ( 'NONE', #36338, #2943, #42462 ) ;
#43156=ADVANCED_FACE ( 'NONE', ( #36827 ), #27452, .F. ) ;
#43168=SHAPE_DEFINITION_REPRESENTATION ( #15828, #15194 ) ;
ENDSEC;
END-ISO-10303-21;
